ISO-10303-21;
HEADER;
/* Generated by software containing ST-Developer
 * from STEP Tools, Inc. (www.steptools.com) 
 */
/* OPTION: using custom renumber hook */

FILE_DESCRIPTION(
/* description */ ('STEP AP242 Edition 2', 'CAx-IF Rec.Pracs.---Representation and Presentation of Product Manufa
cturing Information (PMI)---4.0---2014-10-13', 'CAx-IF Rec.Pracs.---3D Tessellated Geometry---0.4---2014-09-14', '2;1', 'CAx-IF Rec.Pracs.---User Defined Attributes---1.5---2016-08-15'),
/* implementation_level */ '2;1');

FILE_NAME(
/* name */ 'Part 4.step',
/* time_stamp */ '2026-10-07T00:00:55Z',
/* author */ (''),
/* organization */ (''),
/* preprocessor_version */ 'ST-DEVELOPER v20',
/* originating_system */ 'ONSHAPE BY PTC INC, 1.221',
/* authorisation */ '  ');

FILE_SCHEMA (('AP242_MANAGED_MODEL_BASED_3D_ENGINEERING_MIM_LF { 1 0 10303 442 3 1 4 }'));
ENDSEC;

DATA;
#124=SHAPE_REPRESENTATION_RELATIONSHIP('','',#4480,#135);
#135=ADVANCED_BREP_SHAPE_REPRESENTATION('',(#4456),#8543);
#277=CYLINDRICAL_SURFACE('',#4942,0.023);
#278=CYLINDRICAL_SURFACE('',#4945,0.024);
#540=CIRCLE('',#4943,0.023);
#541=CIRCLE('',#4944,0.023);
#542=CIRCLE('',#4946,0.024);
#543=CIRCLE('',#4947,0.024);
#1603=ORIENTED_EDGE('',*,*,#2321,.F.);
#1604=ORIENTED_EDGE('',*,*,#2322,.F.);
#1605=ORIENTED_EDGE('',*,*,#2323,.T.);
#1606=ORIENTED_EDGE('',*,*,#2324,.F.);
#1607=ORIENTED_EDGE('',*,*,#2325,.T.);
#1608=ORIENTED_EDGE('',*,*,#2321,.T.);
#1609=ORIENTED_EDGE('',*,*,#2326,.T.);
#1610=ORIENTED_EDGE('',*,*,#2327,.T.);
#1611=ORIENTED_EDGE('',*,*,#2323,.F.);
#1612=ORIENTED_EDGE('',*,*,#2328,.F.);
#1613=ORIENTED_EDGE('',*,*,#2329,.F.);
#1614=ORIENTED_EDGE('',*,*,#2330,.F.);
#1615=ORIENTED_EDGE('',*,*,#2330,.T.);
#1616=ORIENTED_EDGE('',*,*,#2331,.T.);
#1617=ORIENTED_EDGE('',*,*,#2326,.F.);
#1618=ORIENTED_EDGE('',*,*,#2324,.T.);
#1619=ORIENTED_EDGE('',*,*,#2328,.T.);
#1620=ORIENTED_EDGE('',*,*,#2322,.T.);
#1621=ORIENTED_EDGE('',*,*,#2325,.F.);
#1622=ORIENTED_EDGE('',*,*,#2332,.T.);
#1623=ORIENTED_EDGE('',*,*,#2327,.F.);
#1624=ORIENTED_EDGE('',*,*,#2331,.F.);
#1625=ORIENTED_EDGE('',*,*,#2329,.T.);
#1626=ORIENTED_EDGE('',*,*,#2332,.F.);
#2321=EDGE_CURVE('',#2740,#2741,#2960,.T.);
#2322=EDGE_CURVE('',#2742,#2740,#2961,.T.);
#2323=EDGE_CURVE('',#2742,#2743,#2962,.T.);
#2324=EDGE_CURVE('',#2741,#2743,#2963,.T.);
#2325=EDGE_CURVE('',#2744,#2740,#540,.T.);
#2326=EDGE_CURVE('',#2741,#2745,#541,.T.);
#2327=EDGE_CURVE('',#2745,#2744,#2964,.F.);
#2328=EDGE_CURVE('',#2746,#2742,#542,.T.);
#2329=EDGE_CURVE('',#2747,#2746,#2965,.F.);
#2330=EDGE_CURVE('',#2743,#2747,#543,.T.);
#2331=EDGE_CURVE('',#2747,#2745,#2966,.T.);
#2332=EDGE_CURVE('',#2744,#2746,#2967,.T.);
#2740=VERTEX_POINT('',#8031);
#2741=VERTEX_POINT('',#8032);
#2742=VERTEX_POINT('',#8034);
#2743=VERTEX_POINT('',#8036);
#2744=VERTEX_POINT('',#8040);
#2745=VERTEX_POINT('',#8042);
#2746=VERTEX_POINT('',#8046);
#2747=VERTEX_POINT('',#8048);
#2960=LINE('',#8030,#3138);
#2961=LINE('',#8033,#3139);
#2962=LINE('',#8035,#3140);
#2963=LINE('',#8037,#3141);
#2964=LINE('',#8043,#3142);
#2965=LINE('',#8047,#3143);
#2966=LINE('',#8051,#3144);
#2967=LINE('',#8053,#3145);
#3138=VECTOR('',#6106,1.);
#3139=VECTOR('',#6107,1.);
#3140=VECTOR('',#6108,1.);
#3141=VECTOR('',#6109,1.);
#3142=VECTOR('',#6116,1.);
#3143=VECTOR('',#6121,1.);
#3144=VECTOR('',#6126,1.);
#3145=VECTOR('',#6129,1.);
#3476=EDGE_LOOP('',(#1603,#1604,#1605,#1606));
#3477=EDGE_LOOP('',(#1607,#1608,#1609,#1610));
#3478=EDGE_LOOP('',(#1611,#1612,#1613,#1614));
#3479=EDGE_LOOP('',(#1615,#1616,#1617,#1618));
#3480=EDGE_LOOP('',(#1619,#1620,#1621,#1622));
#3481=EDGE_LOOP('',(#1623,#1624,#1625,#1626));
#3853=FACE_BOUND('',#3476,.T.);
#3854=FACE_BOUND('',#3477,.T.);
#3855=FACE_BOUND('',#3478,.T.);
#3856=FACE_BOUND('',#3479,.T.);
#3857=FACE_BOUND('',#3480,.T.);
#3858=FACE_BOUND('',#3481,.T.);
#4008=PLANE('',#4941);
#4009=PLANE('',#4948);
#4010=PLANE('',#4949);
#4011=PLANE('',#4950);
#4260=ADVANCED_FACE('',(#3853),#4008,.T.);
#4261=ADVANCED_FACE('',(#3854),#277,.F.);
#4262=ADVANCED_FACE('',(#3855),#278,.T.);
#4263=ADVANCED_FACE('',(#3856),#4009,.T.);
#4264=ADVANCED_FACE('',(#3857),#4010,.T.);
#4265=ADVANCED_FACE('',(#3858),#4011,.T.);
#4330=CLOSED_SHELL('',(#4260,#4261,#4262,#4263,#4264,#4265));
#4341=STYLED_ITEM('',(#4352),#4456);
#4352=PRESENTATION_STYLE_ASSIGNMENT((#4368));
#4368=SURFACE_STYLE_USAGE(.BOTH.,#4384);
#4384=SURFACE_SIDE_STYLE('',(#4400));
#4400=SURFACE_STYLE_FILL_AREA(#4416);
#4416=FILL_AREA_STYLE('',(#4432));
#4432=FILL_AREA_STYLE_COLOUR('',#4445);
#4445=COLOUR_RGB('', 0.31764706, 0.68627451, 0.89019608);
#4456=MANIFOLD_SOLID_BREP('Part 4',#4330);
#4468=SHAPE_DEFINITION_REPRESENTATION(#8580,#4480);
#4480=SHAPE_REPRESENTATION('Part 4',(#4484),#8543);
#4484=AXIS2_PLACEMENT_3D('',#6402,#5064,#5065);
#4941=AXIS2_PLACEMENT_3D('',#8029,#6104,#6105);
#4942=AXIS2_PLACEMENT_3D('',#8038,#6110,#6111);
#4943=AXIS2_PLACEMENT_3D('',#8039,#6112,#6113);
#4944=AXIS2_PLACEMENT_3D('',#8041,#6114,#6115);
#4945=AXIS2_PLACEMENT_3D('',#8044,#6117,#6118);
#4946=AXIS2_PLACEMENT_3D('',#8045,#6119,#6120);
#4947=AXIS2_PLACEMENT_3D('',#8049,#6122,#6123);
#4948=AXIS2_PLACEMENT_3D('',#8050,#6124,#6125);
#4949=AXIS2_PLACEMENT_3D('',#8052,#6127,#6128);
#4950=AXIS2_PLACEMENT_3D('',#8054,#6130,#6131);
#5064=DIRECTION('',(0.,0.,1.));
#5065=DIRECTION('',(1.,0.,0.));
#6104=DIRECTION('',(0.,-1.,0.));
#6105=DIRECTION('',(1.,0.,0.));
#6106=DIRECTION('',(0.,0.,-1.));
#6107=DIRECTION('',(1.,0.,0.));
#6108=DIRECTION('',(0.,0.,-1.));
#6109=DIRECTION('',(-1.,0.,0.));
#6110=DIRECTION('',(0.,0.,-1.));
#6111=DIRECTION('',(-1.,0.,0.));
#6112=DIRECTION('',(0.,0.,1.));
#6113=DIRECTION('',(1.,0.,0.));
#6114=DIRECTION('',(0.,0.,-1.));
#6115=DIRECTION('',(-1.,0.,0.));
#6116=DIRECTION('',(0.,0.,-1.));
#6117=DIRECTION('',(0.,0.,-1.));
#6118=DIRECTION('',(-1.,0.,0.));
#6119=DIRECTION('',(0.,0.,1.));
#6120=DIRECTION('',(1.,0.,0.));
#6121=DIRECTION('',(0.,0.,-1.));
#6122=DIRECTION('',(0.,0.,-1.));
#6123=DIRECTION('',(-1.,0.,0.));
#6124=DIRECTION('',(0.,0.,-1.));
#6125=DIRECTION('',(1.,0.,0.));
#6126=DIRECTION('',(-1.,0.,0.));
#6127=DIRECTION('',(0.,0.,1.));
#6128=DIRECTION('',(1.,0.,0.));
#6129=DIRECTION('',(1.,0.,0.));
#6130=DIRECTION('',(0.,-1.,0.));
#6131=DIRECTION('',(1.,0.,0.));
#6402=CARTESIAN_POINT('',(0.,0.,0.));
#8029=CARTESIAN_POINT('',(0.0434268042445183,-0.0746532949430514,0.0110000004));
#8030=CARTESIAN_POINT('',(-0.0221398345609468,-0.0746532949430514,0.0130020004));
#8031=CARTESIAN_POINT('',(-0.0221398345609468,-0.0746532949430514,0.0130000004));
#8032=CARTESIAN_POINT('',(-0.0221398345609468,-0.0746532949430514,-0.0130000004));
#8033=CARTESIAN_POINT('',(0.,-0.0746532949430514,0.0130000004));
#8034=CARTESIAN_POINT('',(-0.0231769772486856,-0.0746532949430514,0.0130000004));
#8035=CARTESIAN_POINT('',(-0.0231769772486856,-0.0746532949430514,0.0130020004));
#8036=CARTESIAN_POINT('',(-0.0231769772486856,-0.0746532949430514,-0.0130000004));
#8037=CARTESIAN_POINT('',(0.,-0.0746532949430514,-0.0130000004));
#8038=CARTESIAN_POINT('',(-5.08934448853094E-19,-0.0684221052,0.0130020004));
#8039=CARTESIAN_POINT('',(-5.08934448853094E-19,-0.0684221052,0.0130000004));
#8040=CARTESIAN_POINT('',(0.0221398345609468,-0.0746532949430514,0.0130000004));
#8041=CARTESIAN_POINT('',(-5.08934448853094E-19,-0.0684221052,-0.0130000004));
#8042=CARTESIAN_POINT('',(0.0221398345609468,-0.0746532949430514,-0.0130000004));
#8043=CARTESIAN_POINT('',(0.0221398345609468,-0.0746532949430514,0.0130020004));
#8044=CARTESIAN_POINT('',(-1.7347234759768E-18,-0.0684221052,0.0130020004));
#8045=CARTESIAN_POINT('',(-1.7347234759768E-18,-0.0684221052,0.0130000004));
#8046=CARTESIAN_POINT('',(0.0231769772486856,-0.0746532949430514,0.0130000004));
#8047=CARTESIAN_POINT('',(0.0231769772486856,-0.0746532949430514,0.0130020004));
#8048=CARTESIAN_POINT('',(0.0231769772486856,-0.0746532949430514,-0.0130000004));
#8049=CARTESIAN_POINT('',(-1.7347234759768E-18,-0.0684221052,-0.0130000004));
#8050=CARTESIAN_POINT('',(0.,0.,-0.0130000004));
#8051=CARTESIAN_POINT('',(0.,-0.0746532949430514,-0.0130000004));
#8052=CARTESIAN_POINT('',(0.,0.,0.0130000004));
#8053=CARTESIAN_POINT('',(0.,-0.0746532949430514,0.0130000004));
#8054=CARTESIAN_POINT('',(0.0434268042445183,-0.0746532949430514,0.0110000004));
#8534=MECHANICAL_DESIGN_GEOMETRIC_PRESENTATION_REPRESENTATION('',(#4341),#8535);
#8535=(
GEOMETRIC_REPRESENTATION_CONTEXT(3)
GLOBAL_UNCERTAINTY_ASSIGNED_CONTEXT((#8547))
GLOBAL_UNIT_ASSIGNED_CONTEXT((#8561,#8560,#8559))
REPRESENTATION_CONTEXT('MAS-680','TOP_LEVEL_ASSEMBLY_PART')
);
#8543=(
GEOMETRIC_REPRESENTATION_CONTEXT(3)
GLOBAL_UNCERTAINTY_ASSIGNED_CONTEXT((#8555))
GLOBAL_UNIT_ASSIGNED_CONTEXT((#8561,#8560,#8559))
REPRESENTATION_CONTEXT('Part 4','COMPONENT_PART')
);
#8547=UNCERTAINTY_MEASURE_WITH_UNIT(LENGTH_MEASURE(1.E-8),#8561,
'DISTANCE_ACCURACY_VALUE','Maximum Tolerance applied to model');
#8555=UNCERTAINTY_MEASURE_WITH_UNIT(LENGTH_MEASURE(1.E-8),#8561,
'DISTANCE_ACCURACY_VALUE','Maximum Tolerance applied to model');
#8559=(
NAMED_UNIT(*)
SI_UNIT($,.STERADIAN.)
SOLID_ANGLE_UNIT()
);
#8560=(
NAMED_UNIT(*)
PLANE_ANGLE_UNIT()
SI_UNIT($,.RADIAN.)
);
#8561=(
LENGTH_UNIT()
NAMED_UNIT(*)
SI_UNIT($,.METRE.)
);
#8580=PRODUCT_DEFINITION_SHAPE('','',#8597);
#8597=PRODUCT_DEFINITION('','',#8621,#8609);
#8609=PRODUCT_DEFINITION_CONTEXT('',#8674,'design');
#8621=PRODUCT_DEFINITION_FORMATION_WITH_SPECIFIED_SOURCE('','',#8645,
 .NOT_KNOWN.);
#8645=PRODUCT('Part 4','Part 4','Part 4',(#8669));
#8669=PRODUCT_CONTEXT('',#8674,'mechanical');
#8674=APPLICATION_CONTEXT('managed model based 3d engineering');
ENDSEC;
END-ISO-10303-21;
